ISO-10303-21;
HEADER;
/* Generated by software containing ST-Developer
 * from STEP Tools, Inc. (www.steptools.com) 
 */

FILE_DESCRIPTION(
/* description */ (''),
/* implementation_level */ '2;1');

FILE_NAME(
/* name */ 'Configuration 1__PD8497.step',
/* time_stamp */ '2026-10-06T10:18:54-07:00',
/* author */ (''),
/* organization */ (''),
/* preprocessor_version */ 'ST-DEVELOPER v20.2',
/* originating_system */ 'Autodesk Translation Framework v15.15.0.0',
/* authorisation */ '');

FILE_SCHEMA (('AUTOMOTIVE_DESIGN { 1 0 10303 214 3 1 1 }'));
ENDSEC;

DATA;
#10=MECHANICAL_DESIGN_GEOMETRIC_PRESENTATION_REPRESENTATION('',(#83),#8445);
#65=SHAPE_REPRESENTATION_RELATIONSHIP('SRR','None',#8486,#74);
#74=ADVANCED_BREP_SHAPE_REPRESENTATION('',(#92),#8438);
#83=STYLED_ITEM('',(#8537),#92);
#92=MANIFOLD_SOLID_BREP('Body1',#4004);
#147=CYLINDRICAL_SURFACE('',#4348,5.25);
#148=CYLINDRICAL_SURFACE('',#4350,3.25);
#149=CYLINDRICAL_SURFACE('',#4355,5.25);
#150=CYLINDRICAL_SURFACE('',#4357,3.25);
#352=FACE_BOUND('',#931,.T.);
#353=FACE_BOUND('',#935,.T.);
#354=FACE_BOUND('',#939,.T.);
#355=FACE_BOUND('',#940,.T.);
#356=FACE_BOUND('',#946,.T.);
#357=FACE_BOUND('',#947,.T.);
#458=CIRCLE('',#4346,5.25);
#459=CIRCLE('',#4347,3.25);
#460=CIRCLE('',#4349,5.25);
#461=CIRCLE('',#4351,3.25);
#462=CIRCLE('',#4353,5.25);
#463=CIRCLE('',#4354,3.25);
#464=CIRCLE('',#4356,5.25);
#465=CIRCLE('',#4358,3.25);
#680=FACE_OUTER_BOUND('',#930,.T.);
#681=FACE_OUTER_BOUND('',#932,.T.);
#682=FACE_OUTER_BOUND('',#933,.T.);
#683=FACE_OUTER_BOUND('',#934,.T.);
#684=FACE_OUTER_BOUND('',#936,.T.);
#685=FACE_OUTER_BOUND('',#937,.T.);
#686=FACE_OUTER_BOUND('',#938,.T.);
#687=FACE_OUTER_BOUND('',#941,.T.);
#688=FACE_OUTER_BOUND('',#942,.T.);
#689=FACE_OUTER_BOUND('',#943,.T.);
#690=FACE_OUTER_BOUND('',#944,.T.);
#691=FACE_OUTER_BOUND('',#945,.T.);
#930=EDGE_LOOP('',(#3305));
#931=EDGE_LOOP('',(#3306));
#932=EDGE_LOOP('',(#3307,#3308,#3309,#3310));
#933=EDGE_LOOP('',(#3311,#3312,#3313,#3314));
#934=EDGE_LOOP('',(#3315));
#935=EDGE_LOOP('',(#3316));
#936=EDGE_LOOP('',(#3317,#3318,#3319,#3320));
#937=EDGE_LOOP('',(#3321,#3322,#3323,#3324));
#938=EDGE_LOOP('',(#3325,#3326,#3327,#3328));
#939=EDGE_LOOP('',(#3329));
#940=EDGE_LOOP('',(#3330));
#941=EDGE_LOOP('',(#3331,#3332,#3333,#3334));
#942=EDGE_LOOP('',(#3335,#3336,#3337,#3338));
#943=EDGE_LOOP('',(#3339,#3340,#3341,#3342));
#944=EDGE_LOOP('',(#3343,#3344,#3345,#3346));
#945=EDGE_LOOP('',(#3347,#3348,#3349,#3350));
#946=EDGE_LOOP('',(#3351));
#947=EDGE_LOOP('',(#3352));
#1211=LINE('',#8042,#1500);
#1212=LINE('',#8045,#1501);
#1213=LINE('',#8055,#1502);
#1214=LINE('',#8058,#1503);
#1215=LINE('',#8063,#1504);
#1216=LINE('',#8065,#1505);
#1217=LINE('',#8067,#1506);
#1218=LINE('',#8068,#1507);
#1219=LINE('',#8071,#1508);
#1220=LINE('',#8073,#1509);
#1221=LINE('',#8074,#1510);
#1222=LINE('',#8077,#1511);
#1223=LINE('',#8078,#1512);
#1224=LINE('',#8081,#1513);
#1225=LINE('',#8082,#1514);
#1226=LINE('',#8084,#1515);
#1500=VECTOR('',#5174,5.25);
#1501=VECTOR('',#5177,3.25);
#1502=VECTOR('',#5190,5.25);
#1503=VECTOR('',#5193,3.25);
#1504=VECTOR('',#5198,10.);
#1505=VECTOR('',#5199,10.);
#1506=VECTOR('',#5200,10.);
#1507=VECTOR('',#5201,10.);
#1508=VECTOR('',#5204,10.);
#1509=VECTOR('',#5205,10.);
#1510=VECTOR('',#5206,10.);
#1511=VECTOR('',#5209,10.);
#1512=VECTOR('',#5210,10.);
#1513=VECTOR('',#5213,10.);
#1514=VECTOR('',#5214,10.);
#1515=VECTOR('',#5217,10.);
#1848=VERTEX_POINT('',#8035);
#1849=VERTEX_POINT('',#8037);
#1850=VERTEX_POINT('',#8040);
#1851=VERTEX_POINT('',#8044);
#1852=VERTEX_POINT('',#8048);
#1853=VERTEX_POINT('',#8050);
#1854=VERTEX_POINT('',#8053);
#1855=VERTEX_POINT('',#8057);
#1856=VERTEX_POINT('',#8061);
#1857=VERTEX_POINT('',#8062);
#1858=VERTEX_POINT('',#8064);
#1859=VERTEX_POINT('',#8066);
#1860=VERTEX_POINT('',#8070);
#1861=VERTEX_POINT('',#8072);
#1862=VERTEX_POINT('',#8076);
#1863=VERTEX_POINT('',#8080);
#2353=EDGE_CURVE('',#1848,#1848,#458,.T.);
#2354=EDGE_CURVE('',#1849,#1849,#459,.T.);
#2355=EDGE_CURVE('',#1850,#1850,#460,.T.);
#2356=EDGE_CURVE('',#1850,#1848,#1211,.T.);
#2357=EDGE_CURVE('',#1849,#1851,#1212,.T.);
#2358=EDGE_CURVE('',#1851,#1851,#461,.T.);
#2359=EDGE_CURVE('',#1852,#1852,#462,.T.);
#2360=EDGE_CURVE('',#1853,#1853,#463,.T.);
#2361=EDGE_CURVE('',#1854,#1854,#464,.T.);
#2362=EDGE_CURVE('',#1854,#1852,#1213,.T.);
#2363=EDGE_CURVE('',#1853,#1855,#1214,.T.);
#2364=EDGE_CURVE('',#1855,#1855,#465,.T.);
#2365=EDGE_CURVE('',#1856,#1857,#1215,.T.);
#2366=EDGE_CURVE('',#1857,#1858,#1216,.T.);
#2367=EDGE_CURVE('',#1858,#1859,#1217,.T.);
#2368=EDGE_CURVE('',#1859,#1856,#1218,.T.);
#2369=EDGE_CURVE('',#1857,#1860,#1219,.T.);
#2370=EDGE_CURVE('',#1861,#1860,#1220,.T.);
#2371=EDGE_CURVE('',#1858,#1861,#1221,.T.);
#2372=EDGE_CURVE('',#1862,#1861,#1222,.T.);
#2373=EDGE_CURVE('',#1859,#1862,#1223,.T.);
#2374=EDGE_CURVE('',#1863,#1862,#1224,.T.);
#2375=EDGE_CURVE('',#1856,#1863,#1225,.T.);
#2376=EDGE_CURVE('',#1860,#1863,#1226,.T.);
#3305=ORIENTED_EDGE('',*,*,#2353,.F.);
#3306=ORIENTED_EDGE('',*,*,#2354,.T.);
#3307=ORIENTED_EDGE('',*,*,#2355,.F.);
#3308=ORIENTED_EDGE('',*,*,#2356,.T.);
#3309=ORIENTED_EDGE('',*,*,#2353,.T.);
#3310=ORIENTED_EDGE('',*,*,#2356,.F.);
#3311=ORIENTED_EDGE('',*,*,#2354,.F.);
#3312=ORIENTED_EDGE('',*,*,#2357,.T.);
#3313=ORIENTED_EDGE('',*,*,#2358,.F.);
#3314=ORIENTED_EDGE('',*,*,#2357,.F.);
#3315=ORIENTED_EDGE('',*,*,#2359,.F.);
#3316=ORIENTED_EDGE('',*,*,#2360,.T.);
#3317=ORIENTED_EDGE('',*,*,#2361,.F.);
#3318=ORIENTED_EDGE('',*,*,#2362,.T.);
#3319=ORIENTED_EDGE('',*,*,#2359,.T.);
#3320=ORIENTED_EDGE('',*,*,#2362,.F.);
#3321=ORIENTED_EDGE('',*,*,#2360,.F.);
#3322=ORIENTED_EDGE('',*,*,#2363,.T.);
#3323=ORIENTED_EDGE('',*,*,#2364,.F.);
#3324=ORIENTED_EDGE('',*,*,#2363,.F.);
#3325=ORIENTED_EDGE('',*,*,#2365,.T.);
#3326=ORIENTED_EDGE('',*,*,#2366,.T.);
#3327=ORIENTED_EDGE('',*,*,#2367,.T.);
#3328=ORIENTED_EDGE('',*,*,#2368,.T.);
#3329=ORIENTED_EDGE('',*,*,#2358,.T.);
#3330=ORIENTED_EDGE('',*,*,#2364,.T.);
#3331=ORIENTED_EDGE('',*,*,#2366,.F.);
#3332=ORIENTED_EDGE('',*,*,#2369,.T.);
#3333=ORIENTED_EDGE('',*,*,#2370,.F.);
#3334=ORIENTED_EDGE('',*,*,#2371,.F.);
#3335=ORIENTED_EDGE('',*,*,#2367,.F.);
#3336=ORIENTED_EDGE('',*,*,#2371,.T.);
#3337=ORIENTED_EDGE('',*,*,#2372,.F.);
#3338=ORIENTED_EDGE('',*,*,#2373,.F.);
#3339=ORIENTED_EDGE('',*,*,#2368,.F.);
#3340=ORIENTED_EDGE('',*,*,#2373,.T.);
#3341=ORIENTED_EDGE('',*,*,#2374,.F.);
#3342=ORIENTED_EDGE('',*,*,#2375,.F.);
#3343=ORIENTED_EDGE('',*,*,#2365,.F.);
#3344=ORIENTED_EDGE('',*,*,#2375,.T.);
#3345=ORIENTED_EDGE('',*,*,#2376,.F.);
#3346=ORIENTED_EDGE('',*,*,#2369,.F.);
#3347=ORIENTED_EDGE('',*,*,#2376,.T.);
#3348=ORIENTED_EDGE('',*,*,#2374,.T.);
#3349=ORIENTED_EDGE('',*,*,#2372,.T.);
#3350=ORIENTED_EDGE('',*,*,#2370,.T.);
#3351=ORIENTED_EDGE('',*,*,#2355,.T.);
#3352=ORIENTED_EDGE('',*,*,#2361,.T.);
#3712=PLANE('',#4345);
#3713=PLANE('',#4352);
#3714=PLANE('',#4359);
#3715=PLANE('',#4360);
#3716=PLANE('',#4361);
#3717=PLANE('',#4362);
#3718=PLANE('',#4363);
#3719=PLANE('',#4364);
#3921=ADVANCED_FACE('',(#680,#352),#3712,.F.);
#3922=ADVANCED_FACE('',(#681),#147,.F.);
#3923=ADVANCED_FACE('',(#682),#148,.F.);
#3924=ADVANCED_FACE('',(#683,#353),#3713,.F.);
#3925=ADVANCED_FACE('',(#684),#149,.F.);
#3926=ADVANCED_FACE('',(#685),#150,.F.);
#3927=ADVANCED_FACE('',(#686,#354,#355),#3714,.F.);
#3928=ADVANCED_FACE('',(#687),#3715,.T.);
#3929=ADVANCED_FACE('',(#688),#3716,.T.);
#3930=ADVANCED_FACE('',(#689),#3717,.T.);
#3931=ADVANCED_FACE('',(#690),#3718,.T.);
#3932=ADVANCED_FACE('',(#691,#356,#357),#3719,.T.);
#4004=CLOSED_SHELL('',(#3921,#3922,#3923,#3924,#3925,#3926,#3927,#3928,
#3929,#3930,#3931,#3932));
#4344=AXIS2_PLACEMENT_3D('',#8033,#5162,#5163);
#4345=AXIS2_PLACEMENT_3D('',#8034,#5164,#5165);
#4346=AXIS2_PLACEMENT_3D('',#8036,#5166,#5167);
#4347=AXIS2_PLACEMENT_3D('',#8038,#5168,#5169);
#4348=AXIS2_PLACEMENT_3D('',#8039,#5170,#5171);
#4349=AXIS2_PLACEMENT_3D('',#8041,#5172,#5173);
#4350=AXIS2_PLACEMENT_3D('',#8043,#5175,#5176);
#4351=AXIS2_PLACEMENT_3D('',#8046,#5178,#5179);
#4352=AXIS2_PLACEMENT_3D('',#8047,#5180,#5181);
#4353=AXIS2_PLACEMENT_3D('',#8049,#5182,#5183);
#4354=AXIS2_PLACEMENT_3D('',#8051,#5184,#5185);
#4355=AXIS2_PLACEMENT_3D('',#8052,#5186,#5187);
#4356=AXIS2_PLACEMENT_3D('',#8054,#5188,#5189);
#4357=AXIS2_PLACEMENT_3D('',#8056,#5191,#5192);
#4358=AXIS2_PLACEMENT_3D('',#8059,#5194,#5195);
#4359=AXIS2_PLACEMENT_3D('',#8060,#5196,#5197);
#4360=AXIS2_PLACEMENT_3D('',#8069,#5202,#5203);
#4361=AXIS2_PLACEMENT_3D('',#8075,#5207,#5208);
#4362=AXIS2_PLACEMENT_3D('',#8079,#5211,#5212);
#4363=AXIS2_PLACEMENT_3D('',#8083,#5215,#5216);
#4364=AXIS2_PLACEMENT_3D('',#8085,#5218,#5219);
#5162=DIRECTION('axis',(0.,0.,1.));
#5163=DIRECTION('refdir',(1.,0.,0.));
#5164=DIRECTION('center_axis',(0.,0.,-1.));
#5165=DIRECTION('ref_axis',(1.,0.,0.));
#5166=DIRECTION('center_axis',(0.,0.,-1.));
#5167=DIRECTION('ref_axis',(1.,0.,0.));
#5168=DIRECTION('center_axis',(0.,0.,-1.));
#5169=DIRECTION('ref_axis',(1.,0.,0.));
#5170=DIRECTION('center_axis',(0.,0.,-1.));
#5171=DIRECTION('ref_axis',(1.,0.,0.));
#5172=DIRECTION('center_axis',(0.,0.,-1.));
#5173=DIRECTION('ref_axis',(1.,0.,0.));
#5174=DIRECTION('',(0.,0.,-1.));
#5175=DIRECTION('center_axis',(0.,0.,-1.));
#5176=DIRECTION('ref_axis',(1.,0.,0.));
#5177=DIRECTION('',(0.,0.,-1.));
#5178=DIRECTION('center_axis',(0.,0.,1.));
#5179=DIRECTION('ref_axis',(1.,0.,0.));
#5180=DIRECTION('center_axis',(0.,0.,-1.));
#5181=DIRECTION('ref_axis',(1.,0.,0.));
#5182=DIRECTION('center_axis',(0.,0.,-1.));
#5183=DIRECTION('ref_axis',(1.,0.,0.));
#5184=DIRECTION('center_axis',(0.,0.,-1.));
#5185=DIRECTION('ref_axis',(1.,0.,0.));
#5186=DIRECTION('center_axis',(0.,0.,-1.));
#5187=DIRECTION('ref_axis',(1.,0.,0.));
#5188=DIRECTION('center_axis',(0.,0.,-1.));
#5189=DIRECTION('ref_axis',(1.,0.,0.));
#5190=DIRECTION('',(0.,0.,-1.));
#5191=DIRECTION('center_axis',(0.,0.,-1.));
#5192=DIRECTION('ref_axis',(1.,0.,0.));
#5193=DIRECTION('',(0.,0.,-1.));
#5194=DIRECTION('center_axis',(0.,0.,1.));
#5195=DIRECTION('ref_axis',(1.,0.,0.));
#5196=DIRECTION('center_axis',(0.,0.,1.));
#5197=DIRECTION('ref_axis',(1.,0.,0.));
#5198=DIRECTION('',(-1.,0.,0.));
#5199=DIRECTION('',(0.,1.,0.));
#5200=DIRECTION('',(1.,0.,0.));
#5201=DIRECTION('',(0.,-1.,0.));
#5202=DIRECTION('center_axis',(-1.,0.,0.));
#5203=DIRECTION('ref_axis',(0.,-1.,0.));
#5204=DIRECTION('',(0.,0.,1.));
#5205=DIRECTION('',(0.,-1.,0.));
#5206=DIRECTION('',(0.,0.,1.));
#5207=DIRECTION('center_axis',(0.,1.,0.));
#5208=DIRECTION('ref_axis',(-1.,0.,0.));
#5209=DIRECTION('',(-1.,0.,0.));
#5210=DIRECTION('',(0.,0.,1.));
#5211=DIRECTION('center_axis',(1.,0.,0.));
#5212=DIRECTION('ref_axis',(0.,1.,0.));
#5213=DIRECTION('',(0.,1.,0.));
#5214=DIRECTION('',(0.,0.,1.));
#5215=DIRECTION('center_axis',(0.,-1.,0.));
#5216=DIRECTION('ref_axis',(1.,0.,0.));
#5217=DIRECTION('',(1.,0.,0.));
#5218=DIRECTION('center_axis',(0.,0.,1.));
#5219=DIRECTION('ref_axis',(1.,0.,0.));
#8033=CARTESIAN_POINT('',(0.,0.,0.));
#8034=CARTESIAN_POINT('Origin',(-23.2259351895987,-0.054016425456016,3.5));
#8035=CARTESIAN_POINT('',(-28.4759351895987,-0.0540164254560154,3.5));
#8036=CARTESIAN_POINT('Origin',(-23.2259351895987,-0.054016425456016,3.5));
#8037=CARTESIAN_POINT('',(-26.4759351895987,-0.0540164254560156,3.5));
#8038=CARTESIAN_POINT('Origin',(-23.2259351895987,-0.054016425456016,3.5));
#8039=CARTESIAN_POINT('Origin',(-23.2259351895987,-0.054016425456016,4.25));
#8040=CARTESIAN_POINT('',(-28.4759351895987,-0.0540164254560154,5.));
#8041=CARTESIAN_POINT('Origin',(-23.2259351895987,-0.054016425456016,5.));
#8042=CARTESIAN_POINT('',(-28.4759351895987,-0.0540164254560154,4.25));
#8043=CARTESIAN_POINT('Origin',(-23.2259351895987,-0.054016425456016,2.5));
#8044=CARTESIAN_POINT('',(-26.4759351895987,-0.0540164254560156,0.));
#8045=CARTESIAN_POINT('',(-26.4759351895987,-0.0540164254560156,2.5));
#8046=CARTESIAN_POINT('Origin',(-23.2259351895987,-0.054016425456016,0.));
#8047=CARTESIAN_POINT('Origin',(14.7740648104013,-0.054016425456016,3.5));
#8048=CARTESIAN_POINT('',(9.52406481040134,-0.0540164254560154,3.5));
#8049=CARTESIAN_POINT('Origin',(14.7740648104013,-0.054016425456016,3.5));
#8050=CARTESIAN_POINT('',(11.5240648104013,-0.0540164254560156,3.5));
#8051=CARTESIAN_POINT('Origin',(14.7740648104013,-0.054016425456016,3.5));
#8052=CARTESIAN_POINT('Origin',(14.7740648104013,-0.054016425456016,4.25));
#8053=CARTESIAN_POINT('',(9.52406481040134,-0.0540164254560154,5.));
#8054=CARTESIAN_POINT('Origin',(14.7740648104013,-0.054016425456016,5.));
#8055=CARTESIAN_POINT('',(9.52406481040134,-0.0540164254560154,4.25));
#8056=CARTESIAN_POINT('Origin',(14.7740648104013,-0.054016425456016,2.5));
#8057=CARTESIAN_POINT('',(11.5240648104013,-0.0540164254560156,0.));
#8058=CARTESIAN_POINT('',(11.5240648104013,-0.0540164254560156,2.5));
#8059=CARTESIAN_POINT('Origin',(14.7740648104013,-0.054016425456016,0.));
#8060=CARTESIAN_POINT('Origin',(-4.22593518959866,-2.55401642545602,0.));
#8061=CARTESIAN_POINT('',(30.7740648104013,-25.054016425456,0.));
#8062=CARTESIAN_POINT('',(-39.2259351895987,-25.054016425456,0.));
#8063=CARTESIAN_POINT('',(30.7740648104013,-25.054016425456,0.));
#8064=CARTESIAN_POINT('',(-39.2259351895987,19.945983574544,0.));
#8065=CARTESIAN_POINT('',(-39.2259351895987,-25.054016425456,0.));
#8066=CARTESIAN_POINT('',(30.7740648104013,19.945983574544,0.));
#8067=CARTESIAN_POINT('',(-39.2259351895987,19.945983574544,0.));
#8068=CARTESIAN_POINT('',(30.7740648104013,19.945983574544,0.));
#8069=CARTESIAN_POINT('Origin',(-39.2259351895987,19.945983574544,0.));
#8070=CARTESIAN_POINT('',(-39.2259351895987,-25.054016425456,5.));
#8071=CARTESIAN_POINT('',(-39.2259351895987,-25.054016425456,0.));
#8072=CARTESIAN_POINT('',(-39.2259351895987,19.945983574544,5.));
#8073=CARTESIAN_POINT('',(-39.2259351895987,-25.054016425456,5.));
#8074=CARTESIAN_POINT('',(-39.2259351895987,19.945983574544,0.));
#8075=CARTESIAN_POINT('Origin',(30.7740648104013,19.945983574544,0.));
#8076=CARTESIAN_POINT('',(30.7740648104013,19.945983574544,5.));
#8077=CARTESIAN_POINT('',(-39.2259351895987,19.945983574544,5.));
#8078=CARTESIAN_POINT('',(30.7740648104013,19.945983574544,0.));
#8079=CARTESIAN_POINT('Origin',(30.7740648104013,-25.054016425456,0.));
#8080=CARTESIAN_POINT('',(30.7740648104013,-25.054016425456,5.));
#8081=CARTESIAN_POINT('',(30.7740648104013,19.945983574544,5.));
#8082=CARTESIAN_POINT('',(30.7740648104013,-25.054016425456,0.));
#8083=CARTESIAN_POINT('Origin',(-39.2259351895987,-25.054016425456,0.));
#8084=CARTESIAN_POINT('',(30.7740648104013,-25.054016425456,5.));
#8085=CARTESIAN_POINT('Origin',(-4.22593518959866,-2.55401642545602,5.));
#8427=UNCERTAINTY_MEASURE_WITH_UNIT(LENGTH_MEASURE(0.01),#8446,
'DISTANCE_ACCURACY_VALUE',
'Maximum model space distance between geometric entities at asserted c
onnectivities');
#8434=UNCERTAINTY_MEASURE_WITH_UNIT(LENGTH_MEASURE(0.01),#8446,
'DISTANCE_ACCURACY_VALUE',
'Maximum model space distance between geometric entities at asserted c
onnectivities');
#8438=(
GEOMETRIC_REPRESENTATION_CONTEXT(3)
GLOBAL_UNCERTAINTY_ASSIGNED_CONTEXT((#8427))
GLOBAL_UNIT_ASSIGNED_CONTEXT((#8446,#8448,#8449))
REPRESENTATION_CONTEXT('','3D')
);
#8445=(
GEOMETRIC_REPRESENTATION_CONTEXT(3)
GLOBAL_UNCERTAINTY_ASSIGNED_CONTEXT((#8434))
GLOBAL_UNIT_ASSIGNED_CONTEXT((#8446,#8448,#8449))
REPRESENTATION_CONTEXT('','3D')
);
#8446=(
LENGTH_UNIT()
NAMED_UNIT(*)
SI_UNIT(.MILLI.,.METRE.)
);
#8448=(
NAMED_UNIT(*)
PLANE_ANGLE_UNIT()
SI_UNIT($,.RADIAN.)
);
#8449=(
NAMED_UNIT(*)
SI_UNIT($,.STERADIAN.)
SOLID_ANGLE_UNIT()
);
#8453=SHAPE_DEFINITION_REPRESENTATION(#8463,#8486);
#8463=PRODUCT_DEFINITION_SHAPE('',$,#8497);
#8486=SHAPE_REPRESENTATION('',(#4344),#8438);
#8493=PRODUCT_DEFINITION_CONTEXT('part definition',#8525,'design');
#8497=PRODUCT_DEFINITION('2026-10-04-20-12-21-923','Configuration 1',#8507,
#8493);
#8507=PRODUCT_DEFINITION_FORMATION('',$,#8530);
#8525=APPLICATION_CONTEXT(
'Core Data for Automotive Mechanical Design Process');
#8526=PRODUCT_CONTEXT('part definition',#8525,'mechanical');
#8530=PRODUCT('2026-10-04-20-12-21-923','Configuration 1',$,(#8526));
#8537=PRESENTATION_STYLE_ASSIGNMENT((#8538));
#8538=SURFACE_STYLE_USAGE(.BOTH.,#8539);
#8539=SURFACE_SIDE_STYLE('',(#8540));
#8540=SURFACE_STYLE_FILL_AREA(#8541);
#8541=FILL_AREA_STYLE('Steel - Satin',(#8542));
#8542=FILL_AREA_STYLE_COLOUR('Steel - Satin',#8543);
#8543=COLOUR_RGB('Steel - Satin', 0.09019608, 0.27058824, 0.51372549);
ENDSEC;
END-ISO-10303-21;
